ISO-10303-21;
HEADER;
/* Generated by software containing ST-Developer
 * from STEP Tools, Inc. (www.steptools.com) 
 */

FILE_DESCRIPTION(
/* description */ ('PAT-054'),
/* implementation_level */ '2;1');

FILE_NAME(
/* name */ 'Cap Screw - M6x25.step',
/* time_stamp */ '2026-10-29T16:38:13-07:00',
/* author */ (''),
/* organization */ (''),
/* preprocessor_version */ 'ST-DEVELOPER v20.2',
/* originating_system */ 'Autodesk Translation Framework v15.17.0.0',
/* authorisation */ '');

FILE_SCHEMA (('AUTOMOTIVE_DESIGN { 1 0 10303 214 3 1 1 }'));
ENDSEC;

DATA;
#10=MECHANICAL_DESIGN_GEOMETRIC_PRESENTATION_REPRESENTATION('',(#957),#33981);
#19=ORIENTED_CLOSED_SHELL('',*,#13073,.F.);
#24=BREP_WITH_VOIDS('Body1',#13072,(#19));
#803=CONICAL_SURFACE('',#14806,0.475,0.785398163397449);
#804=CONICAL_SURFACE('',#14810,0.485,0.785398163397448);
#805=CONICAL_SURFACE('',#14814,0.31,0.463647609000806);
#806=CONICAL_SURFACE('',#14818,0.27,0.785398163397448);
#854=SHAPE_REPRESENTATION_RELATIONSHIP('SRR','None',#34232,#898);
#898=ADVANCED_BREP_SHAPE_REPRESENTATION('',(#24),#33980);
#957=STYLED_ITEM('',(#34524),#24);
#1227=FACE_BOUND('',#3224,.T.);
#1564=PLANE('',#14804);
#1565=PLANE('',#14812);
#1566=PLANE('',#14820);
#1567=PLANE('',#14821);
#1568=PLANE('',#14822);
#1569=PLANE('',#14823);
#1570=PLANE('',#14824);
#1571=PLANE('',#14825);
#1572=PLANE('',#14826);
#1573=PLANE('',#14827);
#1574=PLANE('',#14828);
#2281=FACE_OUTER_BOUND('',#3219,.T.);
#2282=FACE_OUTER_BOUND('',#3220,.T.);
#2283=FACE_OUTER_BOUND('',#3221,.T.);
#2284=FACE_OUTER_BOUND('',#3222,.T.);
#2285=FACE_OUTER_BOUND('',#3223,.T.);
#2286=FACE_OUTER_BOUND('',#3225,.T.);
#2287=FACE_OUTER_BOUND('',#3226,.T.);
#2288=FACE_OUTER_BOUND('',#3227,.T.);
#2289=FACE_OUTER_BOUND('',#3228,.T.);
#2290=FACE_OUTER_BOUND('',#3229,.T.);
#2291=FACE_OUTER_BOUND('',#3230,.T.);
#2292=FACE_OUTER_BOUND('',#3231,.T.);
#2293=FACE_OUTER_BOUND('',#3232,.T.);
#2294=FACE_OUTER_BOUND('',#3233,.T.);
#2295=FACE_OUTER_BOUND('',#3234,.T.);
#2296=FACE_OUTER_BOUND('',#3235,.T.);
#2297=FACE_OUTER_BOUND('',#3236,.T.);
#3219=EDGE_LOOP('',(#11915));
#3220=EDGE_LOOP('',(#11916,#11917,#11918,#11919));
#3221=EDGE_LOOP('',(#11920,#11921,#11922,#11923));
#3222=EDGE_LOOP('',(#11924,#11925,#11926,#11927));
#3223=EDGE_LOOP('',(#11928));
#3224=EDGE_LOOP('',(#11929));
#3225=EDGE_LOOP('',(#11930,#11931,#11932,#11933));
#3226=EDGE_LOOP('',(#11934,#11935,#11936,#11937));
#3227=EDGE_LOOP('',(#11938,#11939,#11940,#11941));
#3228=EDGE_LOOP('',(#11942));
#3229=EDGE_LOOP('',(#11943,#11944,#11945,#11946));
#3230=EDGE_LOOP('',(#11947,#11948,#11949,#11950));
#3231=EDGE_LOOP('',(#11951,#11952,#11953,#11954));
#3232=EDGE_LOOP('',(#11955,#11956,#11957,#11958));
#3233=EDGE_LOOP('',(#11959,#11960,#11961,#11962));
#3234=EDGE_LOOP('',(#11963,#11964,#11965,#11966));
#3235=EDGE_LOOP('',(#11967,#11968,#11969,#11970,#11971,#11972));
#3236=EDGE_LOOP('',(#11973,#11974,#11975,#11976,#11977,#11978));
#4147=LINE('',#33754,#5081);
#4148=LINE('',#33758,#5082);
#4149=LINE('',#33762,#5083);
#4150=LINE('',#33769,#5084);
#4151=LINE('',#33773,#5085);
#4152=LINE('',#33777,#5086);
#4153=LINE('',#33782,#5087);
#4154=LINE('',#33784,#5088);
#4155=LINE('',#33786,#5089);
#4156=LINE('',#33787,#5090);
#4157=LINE('',#33790,#5091);
#4158=LINE('',#33792,#5092);
#4159=LINE('',#33793,#5093);
#4160=LINE('',#33796,#5094);
#4161=LINE('',#33798,#5095);
#4162=LINE('',#33799,#5096);
#4163=LINE('',#33802,#5097);
#4164=LINE('',#33804,#5098);
#4165=LINE('',#33805,#5099);
#4166=LINE('',#33808,#5100);
#4167=LINE('',#33810,#5101);
#4168=LINE('',#33811,#5102);
#4169=LINE('',#33813,#5103);
#4170=LINE('',#33814,#5104);
#5081=VECTOR('',#18298,0.475);
#5082=VECTOR('',#18303,0.5);
#5083=VECTOR('',#18308,0.485);
#5084=VECTOR('',#18317,0.31);
#5085=VECTOR('',#18322,0.3);
#5086=VECTOR('',#18327,0.27);
#5087=VECTOR('',#18332,1.);
#5088=VECTOR('',#18333,1.);
#5089=VECTOR('',#18334,1.);
#5090=VECTOR('',#18335,1.);
#5091=VECTOR('',#18338,1.);
#5092=VECTOR('',#18339,1.);
#5093=VECTOR('',#18340,1.);
#5094=VECTOR('',#18343,1.);
#5095=VECTOR('',#18344,1.);
#5096=VECTOR('',#18345,1.);
#5097=VECTOR('',#18348,1.);
#5098=VECTOR('',#18349,1.);
#5099=VECTOR('',#18350,1.);
#5100=VECTOR('',#18353,1.);
#5101=VECTOR('',#18354,1.);
#5102=VECTOR('',#18355,1.);
#5103=VECTOR('',#18358,1.);
#5104=VECTOR('',#18359,1.);
#5562=CIRCLE('',#14805,0.45);
#5563=CIRCLE('',#14807,0.5);
#5564=CIRCLE('',#14809,0.5);
#5565=CIRCLE('',#14811,0.47);
#5566=CIRCLE('',#14813,0.32);
#5567=CIRCLE('',#14815,0.2942);
#5568=CIRCLE('',#14817,0.2942);
#5569=CIRCLE('',#14819,0.24);
#6724=VERTEX_POINT('',#33749);
#6725=VERTEX_POINT('',#33752);
#6726=VERTEX_POINT('',#33756);
#6727=VERTEX_POINT('',#33760);
#6728=VERTEX_POINT('',#33764);
#6729=VERTEX_POINT('',#33767);
#6730=VERTEX_POINT('',#33771);
#6731=VERTEX_POINT('',#33775);
#6732=VERTEX_POINT('',#33780);
#6733=VERTEX_POINT('',#33781);
#6734=VERTEX_POINT('',#33783);
#6735=VERTEX_POINT('',#33785);
#6736=VERTEX_POINT('',#33789);
#6737=VERTEX_POINT('',#33791);
#6738=VERTEX_POINT('',#33795);
#6739=VERTEX_POINT('',#33797);
#6740=VERTEX_POINT('',#33801);
#6741=VERTEX_POINT('',#33803);
#6742=VERTEX_POINT('',#33807);
#6743=VERTEX_POINT('',#33809);
#8457=EDGE_CURVE('',#6724,#6724,#5562,.T.);
#8458=EDGE_CURVE('',#6725,#6725,#5563,.T.);
#8459=EDGE_CURVE('',#6725,#6724,#4147,.T.);
#8460=EDGE_CURVE('',#6726,#6726,#5564,.T.);
#8461=EDGE_CURVE('',#6726,#6725,#4148,.T.);
#8462=EDGE_CURVE('',#6727,#6727,#5565,.T.);
#8463=EDGE_CURVE('',#6727,#6726,#4149,.T.);
#8464=EDGE_CURVE('',#6728,#6728,#5566,.T.);
#8465=EDGE_CURVE('',#6729,#6729,#5567,.F.);
#8466=EDGE_CURVE('',#6729,#6728,#4150,.T.);
#8467=EDGE_CURVE('',#6730,#6730,#5568,.F.);
#8468=EDGE_CURVE('',#6730,#6729,#4151,.T.);
#8469=EDGE_CURVE('',#6731,#6731,#5569,.T.);
#8470=EDGE_CURVE('',#6731,#6730,#4152,.T.);
#8471=EDGE_CURVE('',#6732,#6733,#4153,.T.);
#8472=EDGE_CURVE('',#6733,#6734,#4154,.T.);
#8473=EDGE_CURVE('',#6734,#6735,#4155,.T.);
#8474=EDGE_CURVE('',#6732,#6735,#4156,.T.);
#8475=EDGE_CURVE('',#6733,#6736,#4157,.T.);
#8476=EDGE_CURVE('',#6736,#6737,#4158,.T.);
#8477=EDGE_CURVE('',#6737,#6734,#4159,.T.);
#8478=EDGE_CURVE('',#6736,#6738,#4160,.T.);
#8479=EDGE_CURVE('',#6738,#6739,#4161,.T.);
#8480=EDGE_CURVE('',#6739,#6737,#4162,.T.);
#8481=EDGE_CURVE('',#6738,#6740,#4163,.T.);
#8482=EDGE_CURVE('',#6740,#6741,#4164,.T.);
#8483=EDGE_CURVE('',#6741,#6739,#4165,.T.);
#8484=EDGE_CURVE('',#6740,#6742,#4166,.T.);
#8485=EDGE_CURVE('',#6742,#6743,#4167,.T.);
#8486=EDGE_CURVE('',#6743,#6741,#4168,.T.);
#8487=EDGE_CURVE('',#6742,#6732,#4169,.T.);
#8488=EDGE_CURVE('',#6735,#6743,#4170,.T.);
#11915=ORIENTED_EDGE('',*,*,#8457,.F.);
#11916=ORIENTED_EDGE('',*,*,#8458,.F.);
#11917=ORIENTED_EDGE('',*,*,#8459,.T.);
#11918=ORIENTED_EDGE('',*,*,#8457,.T.);
#11919=ORIENTED_EDGE('',*,*,#8459,.F.);
#11920=ORIENTED_EDGE('',*,*,#8460,.F.);
#11921=ORIENTED_EDGE('',*,*,#8461,.T.);
#11922=ORIENTED_EDGE('',*,*,#8458,.T.);
#11923=ORIENTED_EDGE('',*,*,#8461,.F.);
#11924=ORIENTED_EDGE('',*,*,#8462,.F.);
#11925=ORIENTED_EDGE('',*,*,#8463,.T.);
#11926=ORIENTED_EDGE('',*,*,#8460,.T.);
#11927=ORIENTED_EDGE('',*,*,#8463,.F.);
#11928=ORIENTED_EDGE('',*,*,#8462,.T.);
#11929=ORIENTED_EDGE('',*,*,#8464,.F.);
#11930=ORIENTED_EDGE('',*,*,#8465,.F.);
#11931=ORIENTED_EDGE('',*,*,#8466,.T.);
#11932=ORIENTED_EDGE('',*,*,#8464,.T.);
#11933=ORIENTED_EDGE('',*,*,#8466,.F.);
#11934=ORIENTED_EDGE('',*,*,#8467,.F.);
#11935=ORIENTED_EDGE('',*,*,#8468,.T.);
#11936=ORIENTED_EDGE('',*,*,#8465,.T.);
#11937=ORIENTED_EDGE('',*,*,#8468,.F.);
#11938=ORIENTED_EDGE('',*,*,#8469,.F.);
#11939=ORIENTED_EDGE('',*,*,#8470,.T.);
#11940=ORIENTED_EDGE('',*,*,#8467,.T.);
#11941=ORIENTED_EDGE('',*,*,#8470,.F.);
#11942=ORIENTED_EDGE('',*,*,#8469,.T.);
#11943=ORIENTED_EDGE('',*,*,#8471,.T.);
#11944=ORIENTED_EDGE('',*,*,#8472,.T.);
#11945=ORIENTED_EDGE('',*,*,#8473,.T.);
#11946=ORIENTED_EDGE('',*,*,#8474,.F.);
#11947=ORIENTED_EDGE('',*,*,#8475,.T.);
#11948=ORIENTED_EDGE('',*,*,#8476,.T.);
#11949=ORIENTED_EDGE('',*,*,#8477,.T.);
#11950=ORIENTED_EDGE('',*,*,#8472,.F.);
#11951=ORIENTED_EDGE('',*,*,#8478,.T.);
#11952=ORIENTED_EDGE('',*,*,#8479,.T.);
#11953=ORIENTED_EDGE('',*,*,#8480,.T.);
#11954=ORIENTED_EDGE('',*,*,#8476,.F.);
#11955=ORIENTED_EDGE('',*,*,#8481,.T.);
#11956=ORIENTED_EDGE('',*,*,#8482,.T.);
#11957=ORIENTED_EDGE('',*,*,#8483,.T.);
#11958=ORIENTED_EDGE('',*,*,#8479,.F.);
#11959=ORIENTED_EDGE('',*,*,#8484,.T.);
#11960=ORIENTED_EDGE('',*,*,#8485,.T.);
#11961=ORIENTED_EDGE('',*,*,#8486,.T.);
#11962=ORIENTED_EDGE('',*,*,#8482,.F.);
#11963=ORIENTED_EDGE('',*,*,#8487,.T.);
#11964=ORIENTED_EDGE('',*,*,#8474,.T.);
#11965=ORIENTED_EDGE('',*,*,#8488,.T.);
#11966=ORIENTED_EDGE('',*,*,#8485,.F.);
#11967=ORIENTED_EDGE('',*,*,#8487,.F.);
#11968=ORIENTED_EDGE('',*,*,#8484,.F.);
#11969=ORIENTED_EDGE('',*,*,#8481,.F.);
#11970=ORIENTED_EDGE('',*,*,#8478,.F.);
#11971=ORIENTED_EDGE('',*,*,#8475,.F.);
#11972=ORIENTED_EDGE('',*,*,#8471,.F.);
#11973=ORIENTED_EDGE('',*,*,#8488,.F.);
#11974=ORIENTED_EDGE('',*,*,#8473,.F.);
#11975=ORIENTED_EDGE('',*,*,#8477,.F.);
#11976=ORIENTED_EDGE('',*,*,#8480,.F.);
#11977=ORIENTED_EDGE('',*,*,#8483,.F.);
#11978=ORIENTED_EDGE('',*,*,#8486,.F.);
#12285=CYLINDRICAL_SURFACE('',#14808,0.5);
#12286=CYLINDRICAL_SURFACE('',#14816,0.2942);
#12993=ADVANCED_FACE('',(#2281),#1564,.T.);
#12994=ADVANCED_FACE('',(#2282),#803,.T.);
#12995=ADVANCED_FACE('',(#2283),#12285,.T.);
#12996=ADVANCED_FACE('',(#2284),#804,.T.);
#12997=ADVANCED_FACE('',(#2285,#1227),#1565,.T.);
#12998=ADVANCED_FACE('',(#2286),#805,.T.);
#12999=ADVANCED_FACE('',(#2287),#12286,.T.);
#13000=ADVANCED_FACE('',(#2288),#806,.T.);
#13001=ADVANCED_FACE('',(#2289),#1566,.T.);
#13002=ADVANCED_FACE('',(#2290),#1567,.F.);
#13003=ADVANCED_FACE('',(#2291),#1568,.F.);
#13004=ADVANCED_FACE('',(#2292),#1569,.F.);
#13005=ADVANCED_FACE('',(#2293),#1570,.F.);
#13006=ADVANCED_FACE('',(#2294),#1571,.F.);
#13007=ADVANCED_FACE('',(#2295),#1572,.F.);
#13008=ADVANCED_FACE('',(#2296),#1573,.F.);
#13009=ADVANCED_FACE('',(#2297),#1574,.F.);
#13072=CLOSED_SHELL('',(#12993,#12994,#12995,#12996,#12997,#12998,#12999,
#13000,#13001));
#13073=CLOSED_SHELL('',(#13002,#13003,#13004,#13005,#13006,#13007,#13008,
#13009));
#14803=AXIS2_PLACEMENT_3D('',#33747,#18288,#18289);
#14804=AXIS2_PLACEMENT_3D('',#33748,#18290,#18291);
#14805=AXIS2_PLACEMENT_3D('',#33750,#18292,#18293);
#14806=AXIS2_PLACEMENT_3D('',#33751,#18294,#18295);
#14807=AXIS2_PLACEMENT_3D('',#33753,#18296,#18297);
#14808=AXIS2_PLACEMENT_3D('',#33755,#18299,#18300);
#14809=AXIS2_PLACEMENT_3D('',#33757,#18301,#18302);
#14810=AXIS2_PLACEMENT_3D('',#33759,#18304,#18305);
#14811=AXIS2_PLACEMENT_3D('',#33761,#18306,#18307);
#14812=AXIS2_PLACEMENT_3D('',#33763,#18309,#18310);
#14813=AXIS2_PLACEMENT_3D('',#33765,#18311,#18312);
#14814=AXIS2_PLACEMENT_3D('',#33766,#18313,#18314);
#14815=AXIS2_PLACEMENT_3D('',#33768,#18315,#18316);
#14816=AXIS2_PLACEMENT_3D('',#33770,#18318,#18319);
#14817=AXIS2_PLACEMENT_3D('',#33772,#18320,#18321);
#14818=AXIS2_PLACEMENT_3D('',#33774,#18323,#18324);
#14819=AXIS2_PLACEMENT_3D('',#33776,#18325,#18326);
#14820=AXIS2_PLACEMENT_3D('',#33778,#18328,#18329);
#14821=AXIS2_PLACEMENT_3D('',#33779,#18330,#18331);
#14822=AXIS2_PLACEMENT_3D('',#33788,#18336,#18337);
#14823=AXIS2_PLACEMENT_3D('',#33794,#18341,#18342);
#14824=AXIS2_PLACEMENT_3D('',#33800,#18346,#18347);
#14825=AXIS2_PLACEMENT_3D('',#33806,#18351,#18352);
#14826=AXIS2_PLACEMENT_3D('',#33812,#18356,#18357);
#14827=AXIS2_PLACEMENT_3D('',#33815,#18360,#18361);
#14828=AXIS2_PLACEMENT_3D('',#33816,#18362,#18363);
#18288=DIRECTION('axis',(0.,0.,1.));
#18289=DIRECTION('refdir',(1.,0.,0.));
#18290=DIRECTION('center_axis',(0.,1.,0.));
#18291=DIRECTION('ref_axis',(0.,0.,1.));
#18292=DIRECTION('center_axis',(0.,-1.,0.));
#18293=DIRECTION('ref_axis',(1.,0.,0.));
#18294=DIRECTION('center_axis',(0.,-1.,0.));
#18295=DIRECTION('ref_axis',(1.,0.,0.));
#18296=DIRECTION('center_axis',(0.,-1.,0.));
#18297=DIRECTION('ref_axis',(1.,0.,0.));
#18298=DIRECTION('',(0.707106781186548,0.707106781186547,8.65956056235494E-17));
#18299=DIRECTION('center_axis',(0.,-1.,0.));
#18300=DIRECTION('ref_axis',(1.,0.,0.));
#18301=DIRECTION('center_axis',(0.,-1.,0.));
#18302=DIRECTION('ref_axis',(1.,0.,0.));
#18303=DIRECTION('',(0.,1.,0.));
#18304=DIRECTION('center_axis',(0.,1.,0.));
#18305=DIRECTION('ref_axis',(1.,0.,0.));
#18306=DIRECTION('center_axis',(0.,-1.,0.));
#18307=DIRECTION('ref_axis',(1.,0.,0.));
#18308=DIRECTION('',(-0.707106781186547,0.707106781186548,-8.65956056235493E-17));
#18309=DIRECTION('center_axis',(0.,-1.,0.));
#18310=DIRECTION('ref_axis',(0.,0.,-1.));
#18311=DIRECTION('center_axis',(0.,-1.,0.));
#18312=DIRECTION('ref_axis',(1.,0.,0.));
#18313=DIRECTION('center_axis',(0.,1.,0.));
#18314=DIRECTION('ref_axis',(1.,0.,0.));
#18315=DIRECTION('center_axis',(0.,1.,0.));
#18316=DIRECTION('ref_axis',(1.,0.,0.));
#18317=DIRECTION('',(-0.447213595499958,0.894427190999916,-5.47678698264203E-17));
#18318=DIRECTION('center_axis',(0.,-1.,0.));
#18319=DIRECTION('ref_axis',(1.,0.,0.));
#18320=DIRECTION('center_axis',(0.,1.,0.));
#18321=DIRECTION('ref_axis',(1.,0.,0.));
#18322=DIRECTION('',(0.,1.,0.));
#18323=DIRECTION('center_axis',(0.,1.,0.));
#18324=DIRECTION('ref_axis',(1.,0.,0.));
#18325=DIRECTION('center_axis',(0.,-1.,0.));
#18326=DIRECTION('ref_axis',(1.,0.,0.));
#18327=DIRECTION('',(-0.707106781186547,0.707106781186548,-8.65956056235493E-17));
#18328=DIRECTION('center_axis',(0.,-1.,0.));
#18329=DIRECTION('ref_axis',(0.,0.,-1.));
#18330=DIRECTION('center_axis',(0.866025403784439,0.,-0.5));
#18331=DIRECTION('ref_axis',(0.5,0.,0.866025403784439));
#18332=DIRECTION('',(-0.5,0.,-0.866025403784439));
#18333=DIRECTION('',(0.,-1.,0.));
#18334=DIRECTION('',(0.5,0.,0.866025403784439));
#18335=DIRECTION('',(0.,-1.,0.));
#18336=DIRECTION('center_axis',(1.92296268638356E-16,0.,-1.));
#18337=DIRECTION('ref_axis',(1.,0.,1.92296268638356E-16));
#18338=DIRECTION('',(-1.,0.,-1.92296268638356E-16));
#18339=DIRECTION('',(0.,-1.,0.));
#18340=DIRECTION('',(1.,0.,1.92296268638356E-16));
#18341=DIRECTION('center_axis',(-0.866025403784439,0.,-0.5));
#18342=DIRECTION('ref_axis',(0.5,0.,-0.866025403784439));
#18343=DIRECTION('',(-0.5,0.,0.866025403784438));
#18344=DIRECTION('',(0.,-1.,0.));
#18345=DIRECTION('',(0.5,0.,-0.866025403784438));
#18346=DIRECTION('center_axis',(-0.866025403784439,0.,0.5));
#18347=DIRECTION('ref_axis',(-0.5,0.,-0.866025403784439));
#18348=DIRECTION('',(0.5,0.,0.866025403784439));
#18349=DIRECTION('',(0.,-1.,0.));
#18350=DIRECTION('',(-0.5,0.,-0.866025403784439));
#18351=DIRECTION('center_axis',(-1.92296268638356E-16,0.,1.));
#18352=DIRECTION('ref_axis',(-1.,0.,-1.92296268638356E-16));
#18353=DIRECTION('',(1.,0.,1.92296268638356E-16));
#18354=DIRECTION('',(0.,-1.,0.));
#18355=DIRECTION('',(-1.,0.,-1.92296268638356E-16));
#18356=DIRECTION('center_axis',(0.866025403784439,0.,0.5));
#18357=DIRECTION('ref_axis',(-0.5,0.,0.866025403784439));
#18358=DIRECTION('',(0.5,0.,-0.866025403784439));
#18359=DIRECTION('',(-0.5,0.,0.866025403784439));
#18360=DIRECTION('center_axis',(0.,1.,0.));
#18361=DIRECTION('ref_axis',(1.,0.,0.));
#18362=DIRECTION('center_axis',(0.,-1.,0.));
#18363=DIRECTION('ref_axis',(0.,0.,-1.));
#33747=CARTESIAN_POINT('',(0.,0.,0.));
#33748=CARTESIAN_POINT('Origin',(0.45,0.6,0.));
#33749=CARTESIAN_POINT('',(-0.45,0.6,-5.51091059616309E-17));
#33750=CARTESIAN_POINT('Origin',(0.,0.6,0.));
#33751=CARTESIAN_POINT('Origin',(0.,0.575,0.));
#33752=CARTESIAN_POINT('',(-0.5,0.55,-6.12323399573677E-17));
#33753=CARTESIAN_POINT('Origin',(0.,0.55,0.));
#33754=CARTESIAN_POINT('',(-0.475,0.575,-5.81707229594993E-17));
#33755=CARTESIAN_POINT('Origin',(0.,0.29,0.));
#33756=CARTESIAN_POINT('',(-0.5,0.0299999999999998,-6.12323399573677E-17));
#33757=CARTESIAN_POINT('Origin',(0.,0.0299999999999998,0.));
#33758=CARTESIAN_POINT('',(-0.5,0.29,-6.12323399573677E-17));
#33759=CARTESIAN_POINT('Origin',(0.,0.0150000000000001,0.));
#33760=CARTESIAN_POINT('',(-0.47,7.11236625150491E-17,-5.75583995599256E-17));
#33761=CARTESIAN_POINT('Origin',(0.,0.,0.));
#33762=CARTESIAN_POINT('',(-0.485,0.0150000000000001,-5.93953697586466E-17));
#33763=CARTESIAN_POINT('Origin',(0.32,0.,0.));
#33764=CARTESIAN_POINT('',(-0.32,-6.93889390390723E-18,-3.91886975727153E-17));
#33765=CARTESIAN_POINT('Origin',(0.,0.,0.));
#33766=CARTESIAN_POINT('Origin',(0.,-0.02,0.));
#33767=CARTESIAN_POINT('',(-0.2942,-0.0515999999999999,3.60291088309151E-17));
#33768=CARTESIAN_POINT('Origin',(0.,-0.0515999999999999,0.));
#33769=CARTESIAN_POINT('',(-0.31,-0.02,-3.7964050773568E-17));
#33770=CARTESIAN_POINT('Origin',(0.,-1.24,0.));
#33771=CARTESIAN_POINT('',(-0.2942,-2.4458,3.60291088309151E-17));
#33772=CARTESIAN_POINT('Origin',(0.,-2.4458,0.));
#33773=CARTESIAN_POINT('',(-0.2942,-1.24,-3.60291088309151E-17));
#33774=CARTESIAN_POINT('Origin',(0.,-2.47,0.));
#33775=CARTESIAN_POINT('',(-0.24,-2.5,-2.93915231795365E-17));
#33776=CARTESIAN_POINT('Origin',(0.,-2.5,0.));
#33777=CARTESIAN_POINT('',(-0.27,-2.47,-3.30654635769785E-17));
#33778=CARTESIAN_POINT('Origin',(0.,-2.5,0.));
#33779=CARTESIAN_POINT('Origin',(0.144337567297406,-0.6,-0.25));
#33780=CARTESIAN_POINT('',(0.288675134594813,-0.6,0.));
#33781=CARTESIAN_POINT('',(0.144337567297406,-0.6,-0.25));
#33782=CARTESIAN_POINT('',(0.288675134594813,-0.6,0.));
#33783=CARTESIAN_POINT('',(0.144337567297406,-0.96,-0.25));
#33784=CARTESIAN_POINT('',(0.144337567297406,-0.6,-0.25));
#33785=CARTESIAN_POINT('',(0.288675134594813,-0.96,0.));
#33786=CARTESIAN_POINT('',(0.288675134594813,-0.96,0.));
#33787=CARTESIAN_POINT('',(0.288675134594813,-0.6,0.));
#33788=CARTESIAN_POINT('Origin',(-0.144337567297406,-0.6,-0.25));
#33789=CARTESIAN_POINT('',(-0.144337567297406,-0.6,-0.25));
#33790=CARTESIAN_POINT('',(0.144337567297406,-0.6,-0.25));
#33791=CARTESIAN_POINT('',(-0.144337567297406,-0.96,-0.25));
#33792=CARTESIAN_POINT('',(-0.144337567297406,-0.6,-0.25));
#33793=CARTESIAN_POINT('',(0.144337567297406,-0.96,-0.25));
#33794=CARTESIAN_POINT('Origin',(-0.288675134594813,-0.6,-8.32667268468867E-17));
#33795=CARTESIAN_POINT('',(-0.288675134594813,-0.6,-3.53525079574969E-17));
#33796=CARTESIAN_POINT('',(-0.144337567297406,-0.6,-0.25));
#33797=CARTESIAN_POINT('',(-0.288675134594813,-0.96,-5.55111512312578E-17));
#33798=CARTESIAN_POINT('',(-0.288675134594813,-0.6,-3.53525079574969E-17));
#33799=CARTESIAN_POINT('',(-0.144337567297406,-0.96,-0.25));
#33800=CARTESIAN_POINT('Origin',(-0.144337567297407,-0.6,0.25));
#33801=CARTESIAN_POINT('',(-0.144337567297407,-0.6,0.25));
#33802=CARTESIAN_POINT('',(-0.288675134594813,-0.6,-3.53525079574969E-17));
#33803=CARTESIAN_POINT('',(-0.144337567297407,-0.96,0.25));
#33804=CARTESIAN_POINT('',(-0.144337567297407,-0.6,0.25));
#33805=CARTESIAN_POINT('',(-0.288675134594813,-0.96,-3.53525079574969E-17));
#33806=CARTESIAN_POINT('Origin',(0.144337567297406,-0.6,0.25));
#33807=CARTESIAN_POINT('',(0.144337567297406,-0.6,0.25));
#33808=CARTESIAN_POINT('',(-0.144337567297407,-0.6,0.25));
#33809=CARTESIAN_POINT('',(0.144337567297406,-0.96,0.25));
#33810=CARTESIAN_POINT('',(0.144337567297406,-0.6,0.25));
#33811=CARTESIAN_POINT('',(-0.144337567297407,-0.96,0.25));
#33812=CARTESIAN_POINT('Origin',(0.288675134594813,-0.6,0.));
#33813=CARTESIAN_POINT('',(0.144337567297406,-0.6,0.25));
#33814=CARTESIAN_POINT('',(0.144337567297406,-0.96,0.25));
#33815=CARTESIAN_POINT('Origin',(0.,-0.6,0.));
#33816=CARTESIAN_POINT('Origin',(0.,-0.96,0.));
#33928=UNCERTAINTY_MEASURE_WITH_UNIT(LENGTH_MEASURE(0.001),#33982,
'DISTANCE_ACCURACY_VALUE',
'Maximum model space distance between geometric entities at asserted c
onnectivities');
#33929=UNCERTAINTY_MEASURE_WITH_UNIT(LENGTH_MEASURE(0.001),#33982,
'DISTANCE_ACCURACY_VALUE',
'Maximum model space distance between geometric entities at asserted c
onnectivities');
#33980=(
GEOMETRIC_REPRESENTATION_CONTEXT(3)
GLOBAL_UNCERTAINTY_ASSIGNED_CONTEXT((#33928))
GLOBAL_UNIT_ASSIGNED_CONTEXT((#33982,#33984,#33985))
REPRESENTATION_CONTEXT('','3D')
);
#33981=(
GEOMETRIC_REPRESENTATION_CONTEXT(3)
GLOBAL_UNCERTAINTY_ASSIGNED_CONTEXT((#33929))
GLOBAL_UNIT_ASSIGNED_CONTEXT((#33982,#33984,#33985))
REPRESENTATION_CONTEXT('','3D')
);
#33982=(
LENGTH_UNIT()
NAMED_UNIT(*)
SI_UNIT(.CENTI.,.METRE.)
);
#33984=(
NAMED_UNIT(*)
PLANE_ANGLE_UNIT()
SI_UNIT($,.RADIAN.)
);
#33985=(
NAMED_UNIT(*)
SI_UNIT($,.STERADIAN.)
SOLID_ANGLE_UNIT()
);
#34036=SHAPE_DEFINITION_REPRESENTATION(#34120,#34232);
#34120=PRODUCT_DEFINITION_SHAPE('',$,#34284);
#34232=SHAPE_REPRESENTATION('',(#14803),#33980);
#34233=PRODUCT_DEFINITION_CONTEXT('part definition',#34388,'design');
#34284=PRODUCT_DEFINITION('Cap Screw - M6x25','Cap Screw - M6x25',#34335,
#34233);
#34335=PRODUCT_DEFINITION_FORMATION('',$,#34440);
#34388=APPLICATION_CONTEXT(
'Core Data for Automotive Mechanical Design Process');
#34389=PRODUCT_CONTEXT('part definition',#34388,'mechanical');
#34440=PRODUCT('Cap Screw - M6x25','Cap Screw - M6x25',
'Cap Screw - M6x25',(#34389));
#34518=COLOUR_RGB('Black',0.12,0.14,0.17);
#34519=FILL_AREA_STYLE_COLOUR('',#34518);
#34520=FILL_AREA_STYLE('',(#34519));
#34521=SURFACE_STYLE_FILL_AREA(#34520);
#34522=SURFACE_SIDE_STYLE('',(#34521));
#34523=SURFACE_STYLE_USAGE(.BOTH.,#34522);
#34524=PRESENTATION_STYLE_ASSIGNMENT((#34523));
ENDSEC;
END-ISO-10303-21;
